ISO-10303-21;
HEADER;
FILE_DESCRIPTION (('STEP AP214'),
    '1' );
FILE_NAME ('Servo-Axe.step',
    '2026-11-01T06:29:40',
    ( '' ),
    ( '' ),
    'SwSTEP 2.0',
    'SolidWorks 2024',
    '' );
FILE_SCHEMA (( 'AUTOMOTIVE_DESIGN' ));
ENDSEC;

DATA;
#73=CARTESIAN_POINT ( 'NONE',  ( 0.000000000000000000, 65.20000000000000284, -5.741599279633704455E-16 ) ) ;
#100=ORIENTED_EDGE ( 'NONE', *, *, #10783, .T. ) ;
#144=FACE_OUTER_BOUND ( 'NONE', #3451, .T. ) ;
#161=AXIS2_PLACEMENT_3D ( 'NONE', #2517, #8811, #5420 ) ;
#184=DIRECTION ( 'NONE',  ( 0.000000000000000000, 0.000000000000000000, 1.000000000000000000 ) ) ;
#208=PRODUCT ( 'Servo-Axe', 'Servo-Axe', '', ( #17249 ) ) ;
#224=ORIENTED_EDGE ( 'NONE', *, *, #18076, .T. ) ;
#225=CARTESIAN_POINT ( 'NONE',  ( 0.000000000000000000, 10.00000000000000000, 0.000000000000000000 ) ) ;
#233=B_SPLINE_CURVE_WITH_KNOTS ( 'NONE', 3,
 ( #2154, #5367, #12797, #3521, #9692, #8463, #14739, #9798, #14639, #306, #11544, #6719, #13012, #17724, #16110, #13117, #516, #14527 ),
 .UNSPECIFIED., .F., .F.,
 ( 4, 2, 2, 2, 2, 2, 2, 2, 4 ),
 ( 0.004721323624227211080, 0.005310725018217473184, 0.005900126412207735288, 0.006489527806197996525, 0.007078929200188269905, 0.007668330594178543284, 0.008257731988168816664, 0.008847133382159089177, 0.009436534776149363424 ),
 .UNSPECIFIED. ) ;
#237=DIRECTION ( 'NONE',  ( 0.000000000000000000, 0.000000000000000000, 1.000000000000000000 ) ) ;
#306=CARTESIAN_POINT ( 'NONE',  ( 2.259918635623968441, 61.98265998586796854, 9.228371864727256124 ) ) ;
#359=CARTESIAN_POINT ( 'NONE',  ( -3.000000000000002220, 60.00000000000000711, 6.000000000000000000 ) ) ;
#475=B_SPLINE_CURVE_WITH_KNOTS ( 'NONE', 3,
 ( #13075, #4904, #12750, #13157, #19000, #3666, #17459, #5011, #3357, #3473, #9633, #15954, #6560, #11281, #9750, #2199, #18370, #657 ),
 .UNSPECIFIED., .F., .F.,
 ( 4, 2, 2, 2, 2, 2, 2, 2, 4 ),
 ( 0.004721323624227206743, 0.005310725018217476653, 0.005900126412207745696, 0.006489527806198015607, 0.007078929200188285517, 0.007668330594178554560, 0.008257731988168825338, 0.008847133382159092646, 0.009436534776149363424 ),
 .UNSPECIFIED. ) ;
#498=ORIENTED_EDGE ( 'NONE', *, *, #10417, .F. ) ;
#516=CARTESIAN_POINT ( 'NONE',  ( 2.999999999999998668, 60.19942049011861940, 9.013878188659973034 ) ) ;
#532=CARTESIAN_POINT ( 'NONE',  ( 3.000000000000000000, 41.00000000000000711, 6.000000000000000000 ) ) ;
#537=CARTESIAN_POINT ( 'NONE',  ( -3.000000000000000000, 41.00000000000000711, 9.013878188659973034 ) ) ;
#556=CARTESIAN_POINT ( 'NONE',  ( 2.980268877975829511, 40.60428768742846728, 9.020512128682495856 ) ) ;
#612=CIRCLE ( 'NONE', #8852, 0.9999999999999983347 ) ;
#647=CARTESIAN_POINT ( 'NONE',  ( 0.3928280596732524055, 38.01925660030116205, 9.493865254640489582 ) ) ;
#656=VECTOR ( 'NONE', #19292, 1000.000000000000000 ) ;
#657=CARTESIAN_POINT ( 'NONE',  ( -3.000000000000000000, 41.00000000000000711, 9.013878188659973034 ) ) ;
#658=VERTEX_POINT ( 'NONE', #16896 ) ;
#660=DIRECTION ( 'NONE',  ( 0.000000000000000000, 0.000000000000000000, 1.000000000000000000 ) ) ;
#699=CARTESIAN_POINT ( 'NONE',  ( 1.224646799147351235E-16, 65.20000000000000284, -0.9999999999999988898 ) ) ;
#713=AXIS2_PLACEMENT_3D ( 'NONE', #15673, #10911, #4930 ) ;
#767=EDGE_CURVE ( 'NONE', #15180, #6572, #6476, .T. ) ;
#793=VECTOR ( 'NONE', #13436, 1000.000000000000000 ) ;
#831=AXIS2_PLACEMENT_3D ( 'NONE', #8730, #9188, #6122 ) ;
#848=AXIS2_PLACEMENT_3D ( 'NONE', #19398, #6769, #17968 ) ;
#878=DIRECTION ( 'NONE',  ( 8.659560562354968603E-17, 0.7071067811865445751, -0.7071067811865504593 ) ) ;
#879=LINE ( 'NONE', #5540, #10619 ) ;
#894=VECTOR ( 'NONE', #17242, 1000.000000000000000 ) ;
#895=FACE_OUTER_BOUND ( 'NONE', #16379, .T. ) ;
#929=ORIENTED_EDGE ( 'NONE', *, *, #11343, .F. ) ;
#1024=EDGE_CURVE ( 'NONE', #9760, #13294, #8830, .T. ) ;
#1060=SURFACE_SIDE_STYLE ('',( #2835 ) ) ;
#1128=CONICAL_SURFACE ( 'NONE', #13367, 0.9999999999999950040, 1.029744258676644320 ) ;
#1181=EDGE_LOOP ( 'NONE', ( #100, #4789, #10034, #9950 ) ) ;
#1203=ORIENTED_EDGE ( 'NONE', *, *, #10783, .F. ) ;
#1262=( LENGTH_UNIT ( ) NAMED_UNIT ( * ) SI_UNIT ( .MILLI., .METRE. ) );
#1319=CIRCLE ( 'NONE', #16839, 1.800000000000000266 ) ;
#1320=AXIS2_PLACEMENT_3D ( 'NONE', #20191, #19881, #5796 ) ;
#1403=APPLICATION_CONTEXT ( 'automotive_design' ) ;
#1442=VECTOR ( 'NONE', #14443, 1000.000000000000000 ) ;
#1509=CARTESIAN_POINT ( 'NONE',  ( -2.601523022692215026, 61.50677485111217635, 9.137549538570182150 ) ) ;
#1545=ORIENTED_EDGE ( 'NONE', *, *, #12654, .T. ) ;
#1557=DIRECTION ( 'NONE',  ( 0.000000000000000000, 0.000000000000000000, 1.000000000000000000 ) ) ;
#1560=EDGE_CURVE ( 'NONE', #13760, #16530, #13725, .T. ) ;
#1640=DIRECTION ( 'NONE',  ( 0.000000000000000000, 0.000000000000000000, -1.000000000000000000 ) ) ;
#1652=CARTESIAN_POINT ( 'NONE',  ( 0.000000000000000000, 38.00000000000000711, 0.9999999999999943379 ) ) ;
#1729=ORIENTED_EDGE ( 'NONE', *, *, #6370, .F. ) ;
#1802=DIRECTION ( 'NONE',  ( -0.000000000000000000, -0.000000000000000000, 1.000000000000000000 ) ) ;
#1829=AXIS2_PLACEMENT_3D ( 'NONE', #13111, #2028, #15783 ) ;
#1900=ORIENTED_EDGE ( 'NONE', *, *, #12305, .F. ) ;
#1981=CARTESIAN_POINT ( 'NONE',  ( 3.000000000000000000, 41.00000000000000711, 9.013878188659973034 ) ) ;
#2028=DIRECTION ( 'NONE',  ( -0.000000000000000000, -1.000000000000000000, -0.000000000000000000 ) ) ;
#2090=VECTOR ( 'NONE', #10357, 1000.000000000000000 ) ;
#2141=CIRCLE ( 'NONE', #18905, 2.999999999999999556 ) ;
#2154=CARTESIAN_POINT ( 'NONE',  ( 1.163414457778310218E-15, 63.00000000000000000, 9.500000000000000000 ) ) ;
#2160=CIRCLE ( 'NONE', #848, 3.000000000000000000 ) ;
#2192=CARTESIAN_POINT ( 'NONE',  ( 0.7808854937525596673, 38.09666348058623697, 9.469847369592788056 ) ) ;
#2194=DIRECTION ( 'NONE',  ( 0.000000000000000000, 0.000000000000000000, 1.000000000000000000 ) ) ;
#2199=CARTESIAN_POINT ( 'NONE',  ( -2.979937318121947509, 40.60126023706489917, 9.020623939867236984 ) ) ;
#2244=CARTESIAN_POINT ( 'NONE',  ( -3.000000000000000000, 41.00000000000000711, 6.000000000000000000 ) ) ;
#2285=CARTESIAN_POINT ( 'NONE',  ( 2.383743612111322463, 39.16804506571254763, 9.196765735797566066 ) ) ;
#2332=DIRECTION ( 'NONE',  ( 0.000000000000000000, 0.000000000000000000, 1.000000000000000000 ) ) ;
#2333=FACE_OUTER_BOUND ( 'NONE', #10143, .T. ) ;
#2367=ORIENTED_EDGE ( 'NONE', *, *, #4353, .T. ) ;
#2428=SURFACE_STYLE_USAGE ( .BOTH. , #1060 ) ;
#2442=DIRECTION ( 'NONE',  ( 1.141265444721583757E-16, -1.000000000000000000, 0.000000000000000000 ) ) ;
#2451=PRODUCT_DEFINITION_CONTEXT ( 'detailed design', #14741, 'design' ) ;
#2472=DIRECTION ( 'NONE',  ( -0.000000000000000000, -0.000000000000000000, 1.000000000000000000 ) ) ;
#2516=DIRECTION ( 'NONE',  ( -0.000000000000000000, -1.000000000000000000, -0.000000000000000000 ) ) ;
#2517=CARTESIAN_POINT ( 'NONE',  ( -1.224646799147350495E-16, 41.00000000000000711, 6.000000000000000000 ) ) ;
#2540=CARTESIAN_POINT ( 'NONE',  ( 3.000000000000000000, 41.00000000000000711, 9.013878188659973034 ) ) ;
#2640=SHAPE_REPRESENTATION_RELATIONSHIP ( 'NONE' , 'NONE' ,  #18121, #13084 ) ;
#2648=VECTOR ( 'NONE', #3850, 1000.000000000000000 ) ;
#2736=DIRECTION ( 'NONE',  ( -0.000000000000000000, -1.000000000000000000, -0.000000000000000000 ) ) ;
#2741=AXIS2_PLACEMENT_3D ( 'NONE', #5042, #3500, #8234 ) ;
#2753=ORIENTED_EDGE ( 'NONE', *, *, #16919, .T. ) ;
#2816=CYLINDRICAL_SURFACE ( 'NONE', #3243, 0.9999999999999965583 ) ;
#2835=SURFACE_STYLE_FILL_AREA ( #16774 ) ;
#2862=CARTESIAN_POINT ( 'NONE',  ( -1.845421771225094876, 62.39699037330763076, 9.323305159997635982 ) ) ;
#2873=EDGE_LOOP ( 'NONE', ( #4370, #224, #18674, #13951 ) ) ;
#2891=EDGE_LOOP ( 'NONE', ( #7975, #1729, #6295, #4329 ) ) ;
#2908=DIRECTION ( 'NONE',  ( 0.000000000000000000, 0.000000000000000000, 1.000000000000000000 ) ) ;
#2955=ORIENTED_EDGE ( 'NONE', *, *, #2998, .F. ) ;
#2998=EDGE_CURVE ( 'NONE', #3066, #10187, #18823, .T. ) ;
#3066=VERTEX_POINT ( 'NONE', #3495 ) ;
#3067=CARTESIAN_POINT ( 'NONE',  ( -3.000000000000002220, 60.19966235751221006, 9.013878188659974811 ) ) ;
#3074=FACE_OUTER_BOUND ( 'NONE', #6651, .T. ) ;
#3138=CARTESIAN_POINT ( 'NONE',  ( 0.000000000000000000, 66.00000000000000000, -5.741599279633704455E-16 ) ) ;
#3151=ORIENTED_EDGE ( 'NONE', *, *, #14163, .F. ) ;
#3160=DIRECTION ( 'NONE',  ( 0.000000000000000000, 0.000000000000000000, 1.000000000000000000 ) ) ;
#3218=EDGE_LOOP ( 'NONE', ( #12689, #4803, #13144, #14286 ) ) ;
#3241=EDGE_CURVE ( 'NONE', #18458, #13936, #4499, .T. ) ;
#3242=CARTESIAN_POINT ( 'NONE',  ( 0.000000000000000000, 38.00000000000000711, -5.741599279633704455E-16 ) ) ;
#3243=AXIS2_PLACEMENT_3D ( 'NONE', #4480, #17049, #2908 ) ;
#3272=AXIS2_PLACEMENT_3D ( 'NONE', #3912, #12066, #10294 ) ;
#3279=CARTESIAN_POINT ( 'NONE',  ( -0.1972064085032595726, 63.00000000000000000, 9.500000000000001776 ) ) ;
#3357=CARTESIAN_POINT ( 'NONE',  ( -1.983673311716146026, 38.74097077230339892, 9.291669371308643122 ) ) ;
#3451=EDGE_LOOP ( 'NONE', ( #12616, #12969, #12450 ) ) ;
#3473=CARTESIAN_POINT ( 'NONE',  ( -2.259918635623970218, 39.01734001413205277, 9.228371864727252571 ) ) ;
#3495=CARTESIAN_POINT ( 'NONE',  ( 1.469576158976824144E-15, 10.00000000000000000, 12.00000000000000178 ) ) ;
#3500=DIRECTION ( 'NONE',  ( 0.000000000000000000, 0.000000000000000000, 1.000000000000000000 ) ) ;
#3521=CARTESIAN_POINT ( 'NONE',  ( 0.7824566857511728868, 62.90282673968097527, 9.469691317190790159 ) ) ;
#3529=ORIENTED_EDGE ( 'NONE', *, *, #5590, .T. ) ;
#3623=CIRCLE ( 'NONE', #5272, 9.500000000000000000 ) ;
#3626=CYLINDRICAL_SURFACE ( 'NONE', #20207, 9.500000000000000000 ) ;
#3666=CARTESIAN_POINT ( 'NONE',  ( -1.334572366541263433, 38.30595095619238322, 9.407584458684455697 ) ) ;
#3669=DIRECTION ( 'NONE',  ( 1.000000000000000000, 0.000000000000000000, -0.000000000000000000 ) ) ;
#3684=EDGE_LOOP ( 'NONE', ( #14648, #7737 ) ) ;
#3700=AXIS2_PLACEMENT_3D ( 'NONE', #18733, #4629, #17193 ) ;
#3761=CIRCLE ( 'NONE', #7054, 0.9999999999999950040 ) ;
#3764=CARTESIAN_POINT ( 'NONE',  ( 0.9714722756524812874, 38.15493332361022283, 9.451944983354378493 ) ) ;
#3805=CARTESIAN_POINT ( 'NONE',  ( -3.000000000000002220, 60.00000000000000711, 6.000000000000000000 ) ) ;
#3850=DIRECTION ( 'NONE',  ( -0.000000000000000000, -0.000000000000000000, 1.000000000000000000 ) ) ;
#3864=ORIENTED_EDGE ( 'NONE', *, *, #13419, .F. ) ;
#3875=PLANE ( 'NONE',  #11938 ) ;
#3907=ORIENTED_EDGE ( 'NONE', *, *, #5767, .F. ) ;
#3912=CARTESIAN_POINT ( 'NONE',  ( 2.999999999999996891, 60.00000000000000711, 6.000000000000000000 ) ) ;
#3958=CARTESIAN_POINT ( 'NONE',  ( 0.000000000000000000, 66.00000000000000000, 0.000000000000000000 ) ) ;
#3977=CIRCLE ( 'NONE', #8263, 1.800000000000000266 ) ;
#4017=CARTESIAN_POINT ( 'NONE',  ( -3.000000000000000000, 41.00000000000000711, 6.000000000000000000 ) ) ;
#4027=ORIENTED_EDGE ( 'NONE', *, *, #14734, .T. ) ;
#4069=CARTESIAN_POINT ( 'NONE',  ( 0.000000000000000000, 66.00000000000000000, -5.741599279633704455E-16 ) ) ;
#4080=( GEOMETRIC_REPRESENTATION_CONTEXT ( 3 ) GLOBAL_UNCERTAINTY_ASSIGNED_CONTEXT ( ( #13586 ) ) GLOBAL_UNIT_ASSIGNED_CONTEXT ( ( #1262, #18399, #8838 ) ) REPRESENTATION_CONTEXT ( 'NONE', 'WORKASPACE' ) );
#4116=AXIS2_PLACEMENT_3D ( 'NONE', #225, #15717, #1640 ) ;
#4183=CARTESIAN_POINT ( 'NONE',  ( 1.163414459189985485E-15, 66.00000000000000000, 9.500000000000000000 ) ) ;
#4219=VERTEX_POINT ( 'NONE', #8740 ) ;
#4241=EDGE_LOOP ( 'NONE', ( #3864, #4523 ) ) ;
#4247=CARTESIAN_POINT ( 'NONE',  ( -3.000000000000003109, 66.00000000000000000, 9.013878188659973034 ) ) ;
#4260=AXIS2_PLACEMENT_3D ( 'NONE', #19732, #5755, #5644 ) ;
#4327=EDGE_CURVE ( 'NONE', #7832, #6379, #16582, .T. ) ;
#4329=ORIENTED_EDGE ( 'NONE', *, *, #12438, .T. ) ;
#4339=EDGE_CURVE ( 'NONE', #15180, #13028, #13283, .T. ) ;
#4353=EDGE_CURVE ( 'NONE', #3066, #19421, #13394, .T. ) ;
#4368=LINE ( 'NONE', #18284, #2090 ) ;
#4370=ORIENTED_EDGE ( 'NONE', *, *, #18854, .F. ) ;
#4454=EDGE_LOOP ( 'NONE', ( #17593, #13861 ) ) ;
#4480=CARTESIAN_POINT ( 'NONE',  ( 0.000000000000000000, 66.00000000000000000, -5.741599279633704455E-16 ) ) ;
#4499=LINE ( 'NONE', #9027, #9600 ) ;
#4500=CARTESIAN_POINT ( 'NONE',  ( 2.999999999999996891, 60.00000000000000711, 9.013878188659974811 ) ) ;
#4523=ORIENTED_EDGE ( 'NONE', *, *, #19935, .F. ) ;
#4527=CARTESIAN_POINT ( 'NONE',  ( -0.7808854937525574469, 62.90333651941379145, 9.469847369592788056 ) ) ;
#4582=CONICAL_SURFACE ( 'NONE', #14492, 1.800000000000000266, 0.7853981633974524978 ) ;
#4597=AXIS2_PLACEMENT_3D ( 'NONE', #4951, #19043, #11334 ) ;
#4629=DIRECTION ( 'NONE',  ( 0.000000000000000000, 1.000000000000000000, 0.000000000000000000 ) ) ;
#4668=LINE ( 'NONE', #10959, #894 ) ;
#4671=ORIENTED_EDGE ( 'NONE', *, *, #12305, .T. ) ;
#4679=COLOUR_RGB ( '', 0.08235294, 0.09019608, 0.10196078) ;
#4724=CARTESIAN_POINT ( 'NONE',  ( -1.734723475976807094E-15, 60.00000000000000711, 6.000000000000000000 ) ) ;
#4750=DIRECTION ( 'NONE',  ( 0.000000000000000000, 0.000000000000000000, 1.000000000000000000 ) ) ;
#4755=FACE_OUTER_BOUND ( 'NONE', #4454, .T. ) ;
#4788=VECTOR ( 'NONE', #15532, 1000.000000000000000 ) ;
#4789=ORIENTED_EDGE ( 'NONE', *, *, #18288, .T. ) ;
#4803=ORIENTED_EDGE ( 'NONE', *, *, #4853, .F. ) ;
#4838=CARTESIAN_POINT ( 'NONE',  ( -1.512611822017144947, 62.62004896476273785, 9.385845453595075938 ) ) ;
#4853=EDGE_CURVE ( 'NONE', #9760, #7832, #612, .T. ) ;
#4871=ADVANCED_FACE ( 'NONE', ( #12298 ), #2816, .F. ) ;
#4904=CARTESIAN_POINT ( 'NONE',  ( -0.1969510947806061563, 38.00000000000000711, 9.500000000000003553 ) ) ;
#4930=DIRECTION ( 'NONE',  ( 0.000000000000000000, 0.000000000000000000, 1.000000000000000000 ) ) ;
#4937=FACE_OUTER_BOUND ( 'NONE', #17666, .T. ) ;
#4951=CARTESIAN_POINT ( 'NONE',  ( 0.000000000000000000, 10.00000000000000000, 0.000000000000000000 ) ) ;
#5011=CARTESIAN_POINT ( 'NONE',  ( -1.831162533324883990, 38.61573685184089300, 9.323294315095141727 ) ) ;
#5040=DIRECTION ( 'NONE',  ( 0.000000000000000000, 0.000000000000000000, 1.000000000000000000 ) ) ;
#5042=CARTESIAN_POINT ( 'NONE',  ( 0.000000000000000000, 0.000000000000000000, 0.000000000000000000 ) ) ;
#5153=CARTESIAN_POINT ( 'NONE',  ( 0.000000000000000000, 38.00000000000000711, -5.741599279633704455E-16 ) ) ;
#5161=DIRECTION ( 'NONE',  ( 0.000000000000000000, 0.000000000000000000, 1.000000000000000000 ) ) ;
#5164=ORIENTED_EDGE ( 'NONE', *, *, #18076, .F. ) ;
#5202=LINE ( 'NONE', #4017, #19099 ) ;
#5254=CIRCLE ( 'NONE', #4597, 12.00000000000000178 ) ;
#5272=AXIS2_PLACEMENT_3D ( 'NONE', #3958, #10053, #2194 ) ;
#5287=DIRECTION ( 'NONE',  ( 0.000000000000000000, 0.000000000000000000, 1.000000000000000000 ) ) ;
#5311=CARTESIAN_POINT ( 'NONE',  ( 2.601523022692213694, 39.49322514888784497, 9.137549538570182150 ) ) ;
#5349=ORIENTED_EDGE ( 'NONE', *, *, #5590, .F. ) ;
#5351=AXIS2_PLACEMENT_3D ( 'NONE', #9876, #12990, #2332 ) ;
#5366=ADVANCED_FACE ( 'NONE', ( #7201, #2333 ), #13399, .T. ) ;
#5367=CARTESIAN_POINT ( 'NONE',  ( 0.1969510947806087375, 63.00000000000001421, 9.500000000000003553 ) ) ;
#5383=ORIENTED_EDGE ( 'NONE', *, *, #19025, .F. ) ;
#5386=LINE ( 'NONE', #532, #656 ) ;
#5420=DIRECTION ( 'NONE',  ( 1.000000000000000000, 0.000000000000000000, 0.000000000000000000 ) ) ;
#5461=ADVANCED_FACE ( 'NONE', ( #16587 ), #13191, .F. ) ;
#5534=( NAMED_UNIT ( * ) PLANE_ANGLE_UNIT ( ) SI_UNIT ( $, .RADIAN. ) );
#5539=DIRECTION ( 'NONE',  ( -0.000000000000000000, -1.000000000000000000, -0.000000000000000000 ) ) ;
#5540=CARTESIAN_POINT ( 'NONE',  ( 1.224646799147349016E-16, 66.00000000000000000, -0.9999999999999972244 ) ) ;
#5590=EDGE_CURVE ( 'NONE', #18458, #4219, #3623, .T. ) ;
#5644=DIRECTION ( 'NONE',  ( 0.000000000000000000, -0.000000000000000000, 1.000000000000000000 ) ) ;
#5755=DIRECTION ( 'NONE',  ( 0.000000000000000000, 1.000000000000000000, 0.000000000000000000 ) ) ;
#5767=EDGE_CURVE ( 'NONE', #15368, #20073, #19123, .T. ) ;
#5796=DIRECTION ( 'NONE',  ( 0.000000000000000000, 0.000000000000000000, 1.000000000000000000 ) ) ;
#5800=CARTESIAN_POINT ( 'NONE',  ( 0.000000000000000000, 10.00000000000000000, -9.500000000000000000 ) ) ;
#5835=VERTEX_POINT ( 'NONE', #8994 ) ;
#5842=ADVANCED_FACE ( 'NONE', ( #13834 ), #7168, .F. ) ;
#5843=PRESENTATION_STYLE_ASSIGNMENT (( #2428 ) ) ;
#5987=PLANE ( 'NONE',  #9178 ) ;
#5997=MECHANICAL_DESIGN_GEOMETRIC_PRESENTATION_REPRESENTATION('',(#19147),#8622);
#6032=CLOSED_SHELL ( 'NONE', ( #6119, #4871, #9006, #9402, #10432, #8769, #13309, #6252, #19524, #5366, #16939, #17317, #11129, #5842, #6490, #12706, #5461, #12050 ) ) ;
#6079=CARTESIAN_POINT ( 'NONE',  ( -0.3928280596732490748, 62.98074339969887347, 9.493865254640493134 ) ) ;
#6105=EDGE_CURVE ( 'NONE', #658, #15368, #5386, .T. ) ;
#6119=ADVANCED_FACE ( 'NONE', ( #9817 ), #4582, .F. ) ;
#6122=DIRECTION ( 'NONE',  ( 0.000000000000000000, 0.000000000000000000, -1.000000000000000000 ) ) ;
#6190=FACE_BOUND ( 'NONE', #4241, .T. ) ;
#6216=FACE_OUTER_BOUND ( 'NONE', #2891, .T. ) ;
#6252=ADVANCED_FACE ( 'NONE', ( #4755 ), #5987, .F. ) ;
#6267=ORIENTED_EDGE ( 'NONE', *, *, #4853, .T. ) ;
#6290=CYLINDRICAL_SURFACE ( 'NONE', #18124, 0.9999999999999965583 ) ;
#6295=ORIENTED_EDGE ( 'NONE', *, *, #10417, .T. ) ;
#6333=SHAPE_DEFINITION_REPRESENTATION ( #8123, #18121 ) ;
#6340=ORIENTED_EDGE ( 'NONE', *, *, #19817, .F. ) ;
#6370=EDGE_CURVE ( 'NONE', #10187, #3066, #5254, .T. ) ;
#6379=VERTEX_POINT ( 'NONE', #12795 ) ;
#6438=CARTESIAN_POINT ( 'NONE',  ( 2.999999999999996891, 60.00000000000000711, 6.000000000000000000 ) ) ;
#6476=LINE ( 'NONE', #18815, #17266 ) ;
#6483=CARTESIAN_POINT ( 'NONE',  ( 1.163414457778310218E-15, 63.00000000000000000, 9.500000000000000000 ) ) ;
#6490=ADVANCED_FACE ( 'NONE', ( #895 ), #18018, .F. ) ;
#6505=ORIENTED_EDGE ( 'NONE', *, *, #9228, .F. ) ;
#6534=CARTESIAN_POINT ( 'NONE',  ( 1.163414460601643398E-15, 38.00000000000000711, 9.500000000000000000 ) ) ;
#6560=CARTESIAN_POINT ( 'NONE',  ( -2.694300560877699535, 39.66622868771214883, 9.110264267939502503 ) ) ;
#6572=VERTEX_POINT ( 'NONE', #14005 ) ;
#6580=VERTEX_POINT ( 'NONE', #10594 ) ;
#6588=LINE ( 'NONE', #10081, #19513 ) ;
#6605=ORIENTED_EDGE ( 'NONE', *, *, #11908, .F. ) ;
#6637=VECTOR ( 'NONE', #19759, 1000.000000000000000 ) ;
#6643=EDGE_CURVE ( 'NONE', #7832, #9760, #10861, .T. ) ;
#6651=EDGE_LOOP ( 'NONE', ( #8290, #10897 ) ) ;
#6684=VECTOR ( 'NONE', #11495, 1000.000000000000000 ) ;
#6687=ORIENTED_EDGE ( 'NONE', *, *, #1560, .T. ) ;
#6719=CARTESIAN_POINT ( 'NONE',  ( 2.600106608147765286, 61.50910620841189314, 9.137947797636652325 ) ) ;
#6769=DIRECTION ( 'NONE',  ( 0.000000000000000000, 0.000000000000000000, 1.000000000000000000 ) ) ;
#6774=CARTESIAN_POINT ( 'NONE',  ( 3.000000000000000888, 40.80033764248782546, 9.013878188659974811 ) ) ;
#6775=EDGE_LOOP ( 'NONE', ( #12739, #18964, #2753, #20264 ) ) ;
#6834=DIRECTION ( 'NONE',  ( 0.000000000000000000, 0.000000000000000000, -1.000000000000000000 ) ) ;
#6867=CARTESIAN_POINT ( 'NONE',  ( 2.257948793614858118, 39.01519438325225053, 9.228844315538687226 ) ) ;
#6960=CARTESIAN_POINT ( 'NONE',  ( 0.1972064085032624869, 38.00000000000002132, 9.500000000000005329 ) ) ;
#6971=CARTESIAN_POINT ( 'NONE',  ( 0.000000000000000000, 38.00000000000000711, -5.741599279633704455E-16 ) ) ;
#7054=AXIS2_PLACEMENT_3D ( 'NONE', #5153, #19258, #5040 ) ;
#7168=CYLINDRICAL_SURFACE ( 'NONE', #17424, 2.999999999999999556 ) ;
#7201=FACE_BOUND ( 'NONE', #3684, .T. ) ;
#7222=CARTESIAN_POINT ( 'NONE',  ( 1.163414459189985485E-15, 66.00000000000000000, 9.500000000000000000 ) ) ;
#7287=CYLINDRICAL_SURFACE ( 'NONE', #831, 12.00000000000000178 ) ;
#7396=CIRCLE ( 'NONE', #17580, 12.00000000000000178 ) ;
#7640=EDGE_CURVE ( 'NONE', #19421, #12712, #15186, .T. ) ;
#7647=ORIENTED_EDGE ( 'NONE', *, *, #6105, .T. ) ;
#7720=CARTESIAN_POINT ( 'NONE',  ( -2.980268877975830399, 60.39571231257155404, 9.020512128682495856 ) ) ;
#7737=ORIENTED_EDGE ( 'NONE', *, *, #16919, .F. ) ;
#7820=CARTESIAN_POINT ( 'NONE',  ( -2.257948793614859451, 61.98480561674775657, 9.228844315538689003 ) ) ;
#7828=ORIENTED_EDGE ( 'NONE', *, *, #12142, .T. ) ;
#7829=ORIENTED_EDGE ( 'NONE', *, *, #12284, .T. ) ;
#7832=VERTEX_POINT ( 'NONE', #699 ) ;
#7839=PRODUCT_DEFINITION ( 'UNKNOWN', '', #16881, #2451 ) ;
#7854=FACE_OUTER_BOUND ( 'NONE', #19203, .T. ) ;
#7931=ORIENTED_EDGE ( 'NONE', *, *, #11994, .F. ) ;
#7975=ORIENTED_EDGE ( 'NONE', *, *, #4353, .F. ) ;
#8084=CARTESIAN_POINT ( 'NONE',  ( 0.000000000000000000, 38.00000000000000711, -5.741599279633704455E-16 ) ) ;
#8100=CIRCLE ( 'NONE', #18293, 9.500000000000000000 ) ;
#8123=PRODUCT_DEFINITION_SHAPE ( 'NONE', 'NONE',  #7839 ) ;
#8131=EDGE_LOOP ( 'NONE', ( #19329, #5349, #10114, #8662, #6605, #1545, #6687, #7828 ) ) ;
#8184=LINE ( 'NONE', #16133, #2648 ) ;
#8197=MANIFOLD_SOLID_BREP ( 'Cut-Extrude1', #6032 ) ;
#8234=DIRECTION ( 'NONE',  ( 1.000000000000000000, 0.000000000000000000, 0.000000000000000000 ) ) ;
#8263=AXIS2_PLACEMENT_3D ( 'NONE', #3138, #9418, #1557 ) ;
#8265=ORIENTED_EDGE ( 'NONE', *, *, #12142, .F. ) ;
#8290=ORIENTED_EDGE ( 'NONE', *, *, #6370, .T. ) ;
#8311=CARTESIAN_POINT ( 'NONE',  ( -3.000000000000002220, 60.00000000000000711, 6.000000000000000000 ) ) ;
#8334=DIRECTION ( 'NONE',  ( -0.000000000000000000, 1.000000000000000000, -0.000000000000000000 ) ) ;
#8407=ORIENTED_EDGE ( 'NONE', *, *, #17010, .F. ) ;
#8430=ORIENTED_EDGE ( 'NONE', *, *, #12654, .F. ) ;
#8463=CARTESIAN_POINT ( 'NONE',  ( 1.334572366541260990, 62.69404904380762389, 9.407584458684453921 ) ) ;
#8502=CARTESIAN_POINT ( 'NONE',  ( -1.734723475976807094E-15, 60.00000000000000711, 6.000000000000000000 ) ) ;
#8522=CARTESIAN_POINT ( 'NONE',  ( 2.204364238465236069E-16, 66.00000000000000000, -1.800000000000000711 ) ) ;
#8529=EDGE_LOOP ( 'NONE', ( #9855, #6505, #8753, #8430, #3907 ) ) ;
#8595=FACE_OUTER_BOUND ( 'NONE', #1181, .T. ) ;
#8622=( GEOMETRIC_REPRESENTATION_CONTEXT ( 3 ) GLOBAL_UNCERTAINTY_ASSIGNED_CONTEXT ( ( #9790 ) ) GLOBAL_UNIT_ASSIGNED_CONTEXT ( ( #12118, #5534, #8920 ) ) REPRESENTATION_CONTEXT ( 'NONE', 'WORKASPACE' ) );
#8662=ORIENTED_EDGE ( 'NONE', *, *, #13419, .T. ) ;
#8729=EDGE_LOOP ( 'NONE', ( #9787, #10748, #4671 ) ) ;
#8730=CARTESIAN_POINT ( 'NONE',  ( 0.000000000000000000, 10.00000000000000000, 0.000000000000000000 ) ) ;
#8740=CARTESIAN_POINT ( 'NONE',  ( 1.163414459189985485E-15, 66.00000000000000000, 9.500000000000000000 ) ) ;
#8753=ORIENTED_EDGE ( 'NONE', *, *, #17010, .T. ) ;
#8769=ADVANCED_FACE ( 'NONE', ( #6216 ), #7287, .T. ) ;
#8770=LINE ( 'NONE', #7222, #6637 ) ;
#8783=ORIENTED_EDGE ( 'NONE', *, *, #19817, .T. ) ;
#8811=DIRECTION ( 'NONE',  ( -0.000000000000000000, -0.000000000000000000, 1.000000000000000000 ) ) ;
#8830=LINE ( 'NONE', #15112, #4788 ) ;
#8838=( NAMED_UNIT ( * ) SI_UNIT ( $, .STERADIAN. ) SOLID_ANGLE_UNIT ( ) );
#8852=AXIS2_PLACEMENT_3D ( 'NONE', #10556, #18281, #15406 ) ;
#8920=( NAMED_UNIT ( * ) SI_UNIT ( $, .STERADIAN. ) SOLID_ANGLE_UNIT ( ) );
#8948=CARTESIAN_POINT ( 'NONE',  ( -3.000000000000003109, 60.00000000000000711, 9.013878188659973034 ) ) ;
#8994=CARTESIAN_POINT ( 'NONE',  ( -3.000000000000002220, 60.00000000000000711, 6.000000000000000000 ) ) ;
#9006=ADVANCED_FACE ( 'NONE', ( #144 ), #1128, .F. ) ;
#9027=CARTESIAN_POINT ( 'NONE',  ( 0.000000000000000000, 66.00000000000000000, -9.500000000000000000 ) ) ;
#9178=AXIS2_PLACEMENT_3D ( 'NONE', #20296, #18747, #11040 ) ;
#9188=DIRECTION ( 'NONE',  ( -0.000000000000000000, -1.000000000000000000, -0.000000000000000000 ) ) ;
#9228=EDGE_CURVE ( 'NONE', #19977, #658, #2160, .T. ) ;
#9271=CARTESIAN_POINT ( 'NONE',  ( 0.000000000000000000, 66.00000000000000000, 0.000000000000000000 ) ) ;
#9287=CARTESIAN_POINT ( 'NONE',  ( 1.469576158976824144E-15, 0.000000000000000000, 12.00000000000000178 ) ) ;
#9379=EDGE_CURVE ( 'NONE', #4219, #18458, #8100, .T. ) ;
#9402=ADVANCED_FACE ( 'NONE', ( #10822 ), #17499, .T. ) ;
#9418=DIRECTION ( 'NONE',  ( -0.000000000000000000, 1.000000000000000000, -0.000000000000000000 ) ) ;
#9521=DIRECTION ( 'NONE',  ( -0.000000000000000000, 1.000000000000000000, -0.000000000000000000 ) ) ;
#9550=DIRECTION ( 'NONE',  ( 1.049727191138612163E-16, 0.5150380749100629263, -0.8571673007021070045 ) ) ;
#9600=VECTOR ( 'NONE', #2736, 1000.000000000000000 ) ;
#9633=CARTESIAN_POINT ( 'NONE',  ( -2.383085342081997293, 39.16728066132458963, 9.196931476227280911 ) ) ;
#9669=CARTESIAN_POINT ( 'NONE',  ( 0.000000000000000000, 66.00000000000000000, 1.799999999999999600 ) ) ;
#9692=CARTESIAN_POINT ( 'NONE',  ( 0.9699764831012678279, 62.84572122215210754, 9.452135968713493597 ) ) ;
#9750=CARTESIAN_POINT ( 'NONE',  ( -2.901926423773061536, 40.21397019809104023, 9.046021540735431188 ) ) ;
#9760=VERTEX_POINT ( 'NONE', #10262 ) ;
#9783=DIRECTION ( 'NONE',  ( -0.000000000000000000, 1.000000000000000000, -0.000000000000000000 ) ) ;
#9787=ORIENTED_EDGE ( 'NONE', *, *, #767, .F. ) ;
#9790=UNCERTAINTY_MEASURE_WITH_UNIT (LENGTH_MEASURE( 1.000000000000000082E-05 ), #12118, 'distance_accuracy_value', 'NONE');
#9798=CARTESIAN_POINT ( 'NONE',  ( 1.831162533324887542, 62.38426314815912832, 9.323294315095143503 ) ) ;
#9817=FACE_OUTER_BOUND ( 'NONE', #6775, .T. ) ;
#9846=ORIENTED_EDGE ( 'NONE', *, *, #7640, .T. ) ;
#9855=ORIENTED_EDGE ( 'NONE', *, *, #6105, .F. ) ;
#9876=CARTESIAN_POINT ( 'NONE',  ( 0.000000000000000000, 10.00000000000000000, 0.000000000000000000 ) ) ;
#9950=ORIENTED_EDGE ( 'NONE', *, *, #19025, .T. ) ;
#10034=ORIENTED_EDGE ( 'NONE', *, *, #9228, .T. ) ;
#10053=DIRECTION ( 'NONE',  ( 0.000000000000000000, 1.000000000000000000, 0.000000000000000000 ) ) ;
#10081=CARTESIAN_POINT ( 'NONE',  ( 0.000000000000000000, 66.00000000000000000, 0.9999999999999958922 ) ) ;
#10086=DIRECTION ( 'NONE',  ( -1.000000000000000000, -1.141265444721583757E-16, 0.000000000000000000 ) ) ;
#10114=ORIENTED_EDGE ( 'NONE', *, *, #3241, .T. ) ;
#10143=EDGE_LOOP ( 'NONE', ( #3529, #15004 ) ) ;
#10187=VERTEX_POINT ( 'NONE', #17361 ) ;
#10248=DIRECTION ( 'NONE',  ( 0.000000000000000000, 0.000000000000000000, 1.000000000000000000 ) ) ;
#10262=CARTESIAN_POINT ( 'NONE',  ( 0.000000000000000000, 65.20000000000000284, 0.9999999999999976685 ) ) ;
#10294=DIRECTION ( 'NONE',  ( -1.597771622610217359E-16, 1.000000000000000000, 0.000000000000000000 ) ) ;
#10357=DIRECTION ( 'NONE',  ( -1.597771622610217359E-16, 1.000000000000000000, -0.000000000000000000 ) ) ;
#10417=EDGE_CURVE ( 'NONE', #10187, #12712, #14240, .T. ) ;
#10432=ADVANCED_FACE ( 'NONE', ( #7854 ), #14351, .T. ) ;
#10552=DIRECTION ( 'NONE',  ( -0.000000000000000000, 1.000000000000000000, -0.000000000000000000 ) ) ;
#10556=CARTESIAN_POINT ( 'NONE',  ( 0.000000000000000000, 65.20000000000000284, -5.741599279633704455E-16 ) ) ;
#10594=CARTESIAN_POINT ( 'NONE',  ( 1.163414459189985485E-15, 10.00000000000000000, 9.500000000000000000 ) ) ;
#10619=VECTOR ( 'NONE', #19835, 1000.000000000000000 ) ;
#10748=ORIENTED_EDGE ( 'NONE', *, *, #4339, .T. ) ;
#10753=FACE_OUTER_BOUND ( 'NONE', #3218, .T. ) ;
#10783=EDGE_CURVE ( 'NONE', #19735, #5835, #2141, .T. ) ;
#10794=VECTOR ( 'NONE', #5539, 1000.000000000000000 ) ;
#10822=FACE_OUTER_BOUND ( 'NONE', #16726, .T. ) ;
#10861=CIRCLE ( 'NONE', #13178, 0.9999999999999983347 ) ;
#10876=AXIS2_PLACEMENT_3D ( 'NONE', #18350, #18450, #13730 ) ;
#10897=ORIENTED_EDGE ( 'NONE', *, *, #2998, .T. ) ;
#10911=DIRECTION ( 'NONE',  ( 0.000000000000000000, 1.000000000000000000, 0.000000000000000000 ) ) ;
#10959=CARTESIAN_POINT ( 'NONE',  ( 2.999999999999996003, 66.00000000000000000, 9.013878188659974811 ) ) ;
#11014=DIRECTION ( 'NONE',  ( 0.000000000000000000, 0.000000000000000000, 1.000000000000000000 ) ) ;
#11040=DIRECTION ( 'NONE',  ( 0.000000000000000000, -0.000000000000000000, 1.000000000000000000 ) ) ;
#11053=B_SPLINE_CURVE_WITH_KNOTS ( 'NONE', 3,
 ( #13889, #3067, #7720, #15677, #12670, #17298, #1509, #18934, #7820, #2862, #4838, #14198, #4527, #6079, #3279, #6483 ),
 .UNSPECIFIED., .F., .F.,
 ( 4, 2, 2, 2, 2, 2, 2, 4 ),
 ( 0.000000000000000000, 0.0005901654530283981324, 0.001180330906056796265, 0.001770496359085194180, 0.002360661812113592530, 0.003540992718170401805, 0.004131158171198806225, 0.004721323624227211080 ),
 .UNSPECIFIED. ) ;
#11129=ADVANCED_FACE ( 'NONE', ( #10753 ), #17043, .F. ) ;
#11281=CARTESIAN_POINT ( 'NONE',  ( -2.844582250340501162, 40.02709031926097083, 9.064464814046603536 ) ) ;
#11297=CIRCLE ( 'NONE', #16272, 0.9999999999999950040 ) ;
#11304=EDGE_LOOP ( 'NONE', ( #8407, #15912, #15440, #17207 ) ) ;
#11334=DIRECTION ( 'NONE',  ( 0.000000000000000000, 0.000000000000000000, 1.000000000000000000 ) ) ;
#11343=EDGE_CURVE ( 'NONE', #14259, #15368, #4668, .T. ) ;
#11461=CARTESIAN_POINT ( 'NONE',  ( 0.000000000000000000, 66.00000000000000000, -5.741599279633704455E-16 ) ) ;
#11495=DIRECTION ( 'NONE',  ( 1.141265444721583757E-16, -1.000000000000000000, 0.000000000000000000 ) ) ;
#11544=CARTESIAN_POINT ( 'NONE',  ( 2.383085342081995517, 61.83271933867543169, 9.196931476227284463 ) ) ;
#11709=CARTESIAN_POINT ( 'NONE',  ( 0.000000000000000000, 0.000000000000000000, -12.00000000000000178 ) ) ;
#11734=CARTESIAN_POINT ( 'NONE',  ( 0.000000000000000000, 38.00000000000000711, 0.9999999999999943379 ) ) ;
#11908=EDGE_CURVE ( 'NONE', #20073, #6580, #8770, .T. ) ;
#11938=AXIS2_PLACEMENT_3D ( 'NONE', #8502, #660, #3669 ) ;
#11994=EDGE_CURVE ( 'NONE', #5835, #16530, #12368, .T. ) ;
#12050=ADVANCED_FACE ( 'NONE', ( #8595 ), #3875, .T. ) ;
#12066=DIRECTION ( 'NONE',  ( 1.000000000000000000, 1.597771622610217359E-16, 0.000000000000000000 ) ) ;
#12118=( LENGTH_UNIT ( ) NAMED_UNIT ( * ) SI_UNIT ( .MILLI., .METRE. ) );
#12142=EDGE_CURVE ( 'NONE', #16530, #12468, #11053, .T. ) ;
#12195=ORIENTED_EDGE ( 'NONE', *, *, #9379, .F. ) ;
#12284=EDGE_CURVE ( 'NONE', #13028, #9760, #6588, .T. ) ;
#12298=FACE_OUTER_BOUND ( 'NONE', #2873, .T. ) ;
#12305=EDGE_CURVE ( 'NONE', #13028, #6572, #3761, .T. ) ;
#12368=LINE ( 'NONE', #8311, #17470 ) ;
#12438=EDGE_CURVE ( 'NONE', #12712, #19421, #7396, .T. ) ;
#12450=ORIENTED_EDGE ( 'NONE', *, *, #18854, .T. ) ;
#12464=PLANE ( 'NONE',  #3700 ) ;
#12468=VERTEX_POINT ( 'NONE', #18613 ) ;
#12488=ORIENTED_EDGE ( 'NONE', *, *, #14163, .T. ) ;
#12499=CARTESIAN_POINT ( 'NONE',  ( 0.000000000000000000, 10.00000000000000000, -12.00000000000000178 ) ) ;
#12564=CARTESIAN_POINT ( 'NONE',  ( 0.000000000000000000, 66.00000000000000000, -5.741599279633704455E-16 ) ) ;
#12616=ORIENTED_EDGE ( 'NONE', *, *, #4339, .F. ) ;
#12651=VECTOR ( 'NONE', #2516, 1000.000000000000000 ) ;
#12654=EDGE_CURVE ( 'NONE', #20073, #13760, #475, .T. ) ;
#12670=CARTESIAN_POINT ( 'NONE',  ( -2.844883903241206546, 60.97223153686513086, 9.064373830433188672 ) ) ;
#12689=ORIENTED_EDGE ( 'NONE', *, *, #4327, .F. ) ;
#12706=ADVANCED_FACE ( 'NONE', ( #15192 ), #16664, .F. ) ;
#12712=VERTEX_POINT ( 'NONE', #11709 ) ;
#12739=ORIENTED_EDGE ( 'NONE', *, *, #6643, .F. ) ;
#12750=CARTESIAN_POINT ( 'NONE',  ( -0.3969782420128915579, 38.01989097161666109, 9.493666329891928157 ) ) ;
#12775=AXIS2_PLACEMENT_3D ( 'NONE', #4069, #10552, #18278 ) ;
#12795=CARTESIAN_POINT ( 'NONE',  ( 2.204364238465236069E-16, 66.00000000000000000, -1.800000000000000711 ) ) ;
#12797=CARTESIAN_POINT ( 'NONE',  ( 0.3969782420128937228, 62.98010902838336023, 9.493666329891928157 ) ) ;
#12829=ORIENTED_EDGE ( 'NONE', *, *, #11343, .T. ) ;
#12910=DIRECTION ( 'NONE',  ( -0.000000000000000000, -1.000000000000000000, -0.000000000000000000 ) ) ;
#12969=ORIENTED_EDGE ( 'NONE', *, *, #767, .T. ) ;
#12990=DIRECTION ( 'NONE',  ( 0.000000000000000000, 1.000000000000000000, 0.000000000000000000 ) ) ;
#13012=CARTESIAN_POINT ( 'NONE',  ( 2.694300560877697759, 61.33377131228787249, 9.110264267939502503 ) ) ;
#13028=VERTEX_POINT ( 'NONE', #1652 ) ;
#13065=CARTESIAN_POINT ( 'NONE',  ( 2.903217335657448661, 40.21902629923274475, 9.045605051663343943 ) ) ;
#13075=CARTESIAN_POINT ( 'NONE',  ( 1.163414460601643398E-15, 38.00000000000000711, 9.500000000000000000 ) ) ;
#13084=ADVANCED_BREP_SHAPE_REPRESENTATION ( '', ( #8197, #2741 ), #4080 ) ;
#13111=CARTESIAN_POINT ( 'NONE',  ( 0.000000000000000000, 66.00000000000000000, 0.000000000000000000 ) ) ;
#13117=CARTESIAN_POINT ( 'NONE',  ( 2.979937318121946177, 60.39873976293512214, 9.020623939867238761 ) ) ;
#13144=ORIENTED_EDGE ( 'NONE', *, *, #1024, .T. ) ;
#13151=CARTESIAN_POINT ( 'NONE',  ( 1.845421771225094210, 38.60300962669240477, 9.323305159997634206 ) ) ;
#13157=CARTESIAN_POINT ( 'NONE',  ( -0.7824566857511718876, 38.09717326031902473, 9.469691317190788382 ) ) ;
#13178=AXIS2_PLACEMENT_3D ( 'NONE', #73, #16183, #184 ) ;
#13191=PLANE ( 'NONE',  #16788 ) ;
#13192=DIRECTION ( 'NONE',  ( -0.000000000000000000, 1.000000000000000000, -0.000000000000000000 ) ) ;
#13243=CARTESIAN_POINT ( 'NONE',  ( 1.163414460601643398E-15, 38.00000000000000711, 9.500000000000000000 ) ) ;
#13280=DIRECTION ( 'NONE',  ( 1.000000000000000000, 0.000000000000000000, 0.000000000000000000 ) ) ;
#13283=LINE ( 'NONE', #11734, #19652 ) ;
#13294=VERTEX_POINT ( 'NONE', #9669 ) ;
#13309=ADVANCED_FACE ( 'NONE', ( #6190, #3074 ), #12464, .T. ) ;
#13367=AXIS2_PLACEMENT_3D ( 'NONE', #3242, #9521, #17150 ) ;
#13394=LINE ( 'NONE', #19632, #10794 ) ;
#13399=PLANE ( 'NONE',  #4260 ) ;
#13400=DIRECTION ( 'NONE',  ( 0.000000000000000000, 0.000000000000000000, 1.000000000000000000 ) ) ;
#13419=EDGE_CURVE ( 'NONE', #13936, #6580, #14890, .T. ) ;
#13436=DIRECTION ( 'NONE',  ( 0.000000000000000000, 1.000000000000000000, 0.000000000000000000 ) ) ;
#13538=CARTESIAN_POINT ( 'NONE',  ( -1.734723475976807094E-15, 60.00000000000000711, 6.000000000000000000 ) ) ;
#13586=UNCERTAINTY_MEASURE_WITH_UNIT (LENGTH_MEASURE( 1.000000000000000082E-05 ), #1262, 'distance_accuracy_value', 'NONE');
#13725=LINE ( 'NONE', #4247, #793 ) ;
#13730=DIRECTION ( 'NONE',  ( 0.000000000000000000, 0.000000000000000000, 1.000000000000000000 ) ) ;
#13760=VERTEX_POINT ( 'NONE', #537 ) ;
#13834=FACE_OUTER_BOUND ( 'NONE', #15865, .T. ) ;
#13861=ORIENTED_EDGE ( 'NONE', *, *, #7640, .F. ) ;
#13889=CARTESIAN_POINT ( 'NONE',  ( -3.000000000000003109, 60.00000000000000711, 9.013878188659973034 ) ) ;
#13912=DIRECTION ( 'NONE',  ( 0.000000000000000000, 1.000000000000000000, 0.000000000000000000 ) ) ;
#13936=VERTEX_POINT ( 'NONE', #5800 ) ;
#13951=ORIENTED_EDGE ( 'NONE', *, *, #12284, .F. ) ;
#14005=CARTESIAN_POINT ( 'NONE',  ( 1.224646799147347044E-16, 38.00000000000000711, -0.9999999999999956701 ) ) ;
#14163=EDGE_CURVE ( 'NONE', #12468, #14259, #233, .T. ) ;
#14198=CARTESIAN_POINT ( 'NONE',  ( -0.9714722756524757363, 62.84506667638981270, 9.451944983354374941 ) ) ;
#14240=LINE ( 'NONE', #12499, #1442 ) ;
#14259=VERTEX_POINT ( 'NONE', #4500 ) ;
#14286=ORIENTED_EDGE ( 'NONE', *, *, #17332, .T. ) ;
#14351=CYLINDRICAL_SURFACE ( 'NONE', #4116, 12.00000000000000178 ) ;
#14413=VECTOR ( 'NONE', #878, 1000.000000000000000 ) ;
#14437=FACE_OUTER_BOUND ( 'NONE', #8131, .T. ) ;
#14443=DIRECTION ( 'NONE',  ( -0.000000000000000000, -1.000000000000000000, -0.000000000000000000 ) ) ;
#14492=AXIS2_PLACEMENT_3D ( 'NONE', #11461, #19181, #5287 ) ;
#14527=CARTESIAN_POINT ( 'NONE',  ( 2.999999999999996891, 60.00000000000000711, 9.013878188659974811 ) ) ;
#14639=CARTESIAN_POINT ( 'NONE',  ( 1.983673311716144694, 62.25902922769662240, 9.291669371308648451 ) ) ;
#14646=CARTESIAN_POINT ( 'NONE',  ( 0.000000000000000000, 66.00000000000000000, 0.000000000000000000 ) ) ;
#14648=ORIENTED_EDGE ( 'NONE', *, *, #17332, .F. ) ;
#14688=CARTESIAN_POINT ( 'NONE',  ( 2.693790225569809849, 39.66504951222130870, 9.110418847747206783 ) ) ;
#14699=LINE ( 'NONE', #359, #6684 ) ;
#14734=EDGE_CURVE ( 'NONE', #4219, #12468, #16663, .T. ) ;
#14739=CARTESIAN_POINT ( 'NONE',  ( 1.507804506096818820, 62.60084458484482894, 9.381017998102993971 ) ) ;
#14741=APPLICATION_CONTEXT ( 'automotive_design' ) ;
#14890=CIRCLE ( 'NONE', #5351, 9.500000000000000000 ) ;
#15004=ORIENTED_EDGE ( 'NONE', *, *, #9379, .T. ) ;
#15112=CARTESIAN_POINT ( 'NONE',  ( 0.000000000000000000, 66.00000000000000000, 1.799999999999999600 ) ) ;
#15180=VERTEX_POINT ( 'NONE', #15613 ) ;
#15186=CIRCLE ( 'NONE', #1320, 12.00000000000000178 ) ;
#15192=FACE_OUTER_BOUND ( 'NONE', #8529, .T. ) ;
#15295=DIRECTION ( 'NONE',  ( -0.000000000000000000, -0.000000000000000000, 1.000000000000000000 ) ) ;
#15368=VERTEX_POINT ( 'NONE', #2540 ) ;
#15406=DIRECTION ( 'NONE',  ( 0.000000000000000000, 0.000000000000000000, 1.000000000000000000 ) ) ;
#15429=CARTESIAN_POINT ( 'NONE',  ( 0.000000000000000000, 0.000000000000000000, 0.000000000000000000 ) ) ;
#15440=ORIENTED_EDGE ( 'NONE', *, *, #11994, .T. ) ;
#15532=DIRECTION ( 'NONE',  ( 0.000000000000000000, 0.7071067811865445751, 0.7071067811865504593 ) ) ;
#15613=CARTESIAN_POINT ( 'NONE',  ( -7.005190481990339112E-15, 37.39913938097243573, -5.741599279633704455E-16 ) ) ;
#15673=CARTESIAN_POINT ( 'NONE',  ( 0.000000000000000000, 10.00000000000000000, 0.000000000000000000 ) ) ;
#15677=CARTESIAN_POINT ( 'NONE',  ( -2.903217335657449993, 60.78097370076725525, 9.045605051663343943 ) ) ;
#15717=DIRECTION ( 'NONE',  ( -0.000000000000000000, -1.000000000000000000, -0.000000000000000000 ) ) ;
#15783=DIRECTION ( 'NONE',  ( 0.000000000000000000, 0.000000000000000000, -1.000000000000000000 ) ) ;
#15865=EDGE_LOOP ( 'NONE', ( #7931, #1203, #8783, #3151, #8265 ) ) ;
#15912=ORIENTED_EDGE ( 'NONE', *, *, #18288, .F. ) ;
#15944=ORIENTED_EDGE ( 'NONE', *, *, #5767, .T. ) ;
#15954=CARTESIAN_POINT ( 'NONE',  ( -2.600106608147766174, 39.49089379158813529, 9.137947797636652325 ) ) ;
#16110=CARTESIAN_POINT ( 'NONE',  ( 2.901926423773059760, 60.78602980190899530, 9.046021540735432964 ) ) ;
#16133=CARTESIAN_POINT ( 'NONE',  ( 2.999999999999996891, 60.00000000000000711, 6.000000000000000000 ) ) ;
#16183=DIRECTION ( 'NONE',  ( -0.000000000000000000, 1.000000000000000000, -0.000000000000000000 ) ) ;
#16272=AXIS2_PLACEMENT_3D ( 'NONE', #6971, #16554, #10248 ) ;
#16357=CARTESIAN_POINT ( 'NONE',  ( 2.844883903241205214, 40.02776846313489045, 9.064373830433188672 ) ) ;
#16379=EDGE_LOOP ( 'NONE', ( #6340, #5383, #7647, #929 ) ) ;
#16495=AXIS2_PLACEMENT_3D ( 'NONE', #8084, #18981, #237 ) ;
#16530=VERTEX_POINT ( 'NONE', #8948 ) ;
#16554=DIRECTION ( 'NONE',  ( -0.000000000000000000, 1.000000000000000000, -0.000000000000000000 ) ) ;
#16582=LINE ( 'NONE', #8522, #14413 ) ;
#16587=FACE_OUTER_BOUND ( 'NONE', #11304, .T. ) ;
#16663=LINE ( 'NONE', #4183, #12651 ) ;
#16664=CYLINDRICAL_SURFACE ( 'NONE', #161, 3.000000000000000000 ) ;
#16726=EDGE_LOOP ( 'NONE', ( #12195, #4027, #12488, #12829, #15944, #17113, #20045, #18766 ) ) ;
#16774=FILL_AREA_STYLE ('',( #19932 ) ) ;
#16788=AXIS2_PLACEMENT_3D ( 'NONE', #3805, #10086, #2442 ) ;
#16839=AXIS2_PLACEMENT_3D ( 'NONE', #19536, #13192, #13400 ) ;
#16881=PRODUCT_DEFINITION_FORMATION_WITH_SPECIFIED_SOURCE ( 'ANY', '', #208, .NOT_KNOWN. ) ;
#16896=CARTESIAN_POINT ( 'NONE',  ( 3.000000000000000000, 41.00000000000000711, 6.000000000000000000 ) ) ;
#16919=EDGE_CURVE ( 'NONE', #6379, #13294, #3977, .T. ) ;
#16939=ADVANCED_FACE ( 'NONE', ( #19392 ), #19752, .F. ) ;
#17010=EDGE_CURVE ( 'NONE', #19977, #13760, #5202, .T. ) ;
#17043=CONICAL_SURFACE ( 'NONE', #12775, 1.800000000000000266, 0.7853981633974524978 ) ;
#17049=DIRECTION ( 'NONE',  ( -0.000000000000000000, 1.000000000000000000, -0.000000000000000000 ) ) ;
#17113=ORIENTED_EDGE ( 'NONE', *, *, #11908, .T. ) ;
#17150=DIRECTION ( 'NONE',  ( 0.000000000000000000, 0.000000000000000000, 1.000000000000000000 ) ) ;
#17193=DIRECTION ( 'NONE',  ( 0.000000000000000000, -0.000000000000000000, 1.000000000000000000 ) ) ;
#17207=ORIENTED_EDGE ( 'NONE', *, *, #1560, .F. ) ;
#17242=DIRECTION ( 'NONE',  ( -0.000000000000000000, -1.000000000000000000, -0.000000000000000000 ) ) ;
#17249=PRODUCT_CONTEXT ( 'NONE', #1403, 'mechanical' ) ;
#17266=VECTOR ( 'NONE', #9550, 1000.000000000000114 ) ;
#17298=CARTESIAN_POINT ( 'NONE',  ( -2.693790225569811625, 61.33495048777871261, 9.110418847747206783 ) ) ;
#17317=ADVANCED_FACE ( 'NONE', ( #4937 ), #6290, .F. ) ;
#17332=EDGE_CURVE ( 'NONE', #13294, #6379, #1319, .T. ) ;
#17361=CARTESIAN_POINT ( 'NONE',  ( 0.000000000000000000, 10.00000000000000000, -12.00000000000000178 ) ) ;
#17424=AXIS2_PLACEMENT_3D ( 'NONE', #13538, #15295, #18270 ) ;
#17459=CARTESIAN_POINT ( 'NONE',  ( -1.507804506096813046, 38.39915541515519237, 9.381017998102995747 ) ) ;
#17470=VECTOR ( 'NONE', #1802, 1000.000000000000000 ) ;
#17499=CYLINDRICAL_SURFACE ( 'NONE', #1829, 9.500000000000000000 ) ;
#17580=AXIS2_PLACEMENT_3D ( 'NONE', #15429, #18909, #3160 ) ;
#17593=ORIENTED_EDGE ( 'NONE', *, *, #12438, .F. ) ;
#17666=EDGE_LOOP ( 'NONE', ( #5164, #1900, #7829, #6267 ) ) ;
#17724=CARTESIAN_POINT ( 'NONE',  ( 2.844582250340499385, 60.97290968073905759, 9.064464814046607088 ) ) ;
#17867=CARTESIAN_POINT ( 'NONE',  ( 1.512611822017149166, 38.37995103523728346, 9.385845453595075938 ) ) ;
#17968=DIRECTION ( 'NONE',  ( 1.000000000000000000, 0.000000000000000000, 0.000000000000000000 ) ) ;
#17999=DIRECTION ( 'NONE',  ( 0.000000000000000000, 0.5150380749100629263, 0.8571673007021070045 ) ) ;
#18018=PLANE ( 'NONE',  #3272 ) ;
#18076=EDGE_CURVE ( 'NONE', #6572, #7832, #879, .T. ) ;
#18121=SHAPE_REPRESENTATION ( 'Servo-Axe', ( #2741 ), #4080 ) ;
#18124=AXIS2_PLACEMENT_3D ( 'NONE', #12564, #9783, #5161 ) ;
#18270=DIRECTION ( 'NONE',  ( 1.000000000000000000, 0.000000000000000000, 0.000000000000000000 ) ) ;
#18278=DIRECTION ( 'NONE',  ( 0.000000000000000000, 0.000000000000000000, 1.000000000000000000 ) ) ;
#18281=DIRECTION ( 'NONE',  ( -0.000000000000000000, 1.000000000000000000, -0.000000000000000000 ) ) ;
#18284=CARTESIAN_POINT ( 'NONE',  ( 2.999999999999996891, 60.00000000000000711, 6.000000000000000000 ) ) ;
#18288=EDGE_CURVE ( 'NONE', #5835, #19977, #14699, .T. ) ;
#18293=AXIS2_PLACEMENT_3D ( 'NONE', #9271, #13912, #4750 ) ;
#18350=CARTESIAN_POINT ( 'NONE',  ( 0.000000000000000000, 10.00000000000000000, 0.000000000000000000 ) ) ;
#18370=CARTESIAN_POINT ( 'NONE',  ( -3.000000000000001776, 40.80057950988138771, 9.013878188659973034 ) ) ;
#18399=( NAMED_UNIT ( * ) PLANE_ANGLE_UNIT ( ) SI_UNIT ( $, .RADIAN. ) );
#18450=DIRECTION ( 'NONE',  ( 0.000000000000000000, 1.000000000000000000, 0.000000000000000000 ) ) ;
#18458=VERTEX_POINT ( 'NONE', #19165 ) ;
#18613=CARTESIAN_POINT ( 'NONE',  ( 1.163414457778310218E-15, 63.00000000000000000, 9.500000000000000000 ) ) ;
#18674=ORIENTED_EDGE ( 'NONE', *, *, #6643, .T. ) ;
#18733=CARTESIAN_POINT ( 'NONE',  ( 0.000000000000000000, 10.00000000000000000, 0.000000000000000000 ) ) ;
#18747=DIRECTION ( 'NONE',  ( 0.000000000000000000, 1.000000000000000000, 0.000000000000000000 ) ) ;
#18766=ORIENTED_EDGE ( 'NONE', *, *, #3241, .F. ) ;
#18815=CARTESIAN_POINT ( 'NONE',  ( 1.224646799147347044E-16, 38.00000000000000711, -0.9999999999999956701 ) ) ;
#18823=CIRCLE ( 'NONE', #713, 12.00000000000000178 ) ;
#18854=EDGE_CURVE ( 'NONE', #6572, #13028, #11297, .T. ) ;
#18905=AXIS2_PLACEMENT_3D ( 'NONE', #4724, #11014, #13280 ) ;
#18909=DIRECTION ( 'NONE',  ( 0.000000000000000000, 1.000000000000000000, 0.000000000000000000 ) ) ;
#18934=CARTESIAN_POINT ( 'NONE',  ( -2.383743612111324239, 61.83195493428745237, 9.196765735797573171 ) ) ;
#18964=ORIENTED_EDGE ( 'NONE', *, *, #4327, .T. ) ;
#18981=DIRECTION ( 'NONE',  ( -0.000000000000000000, 1.000000000000000000, -0.000000000000000000 ) ) ;
#19000=CARTESIAN_POINT ( 'NONE',  ( -0.9699764831012689381, 38.15427877784792088, 9.452135968713491820 ) ) ;
#19025=EDGE_CURVE ( 'NONE', #658, #19735, #4368, .T. ) ;
#19043=DIRECTION ( 'NONE',  ( 0.000000000000000000, 1.000000000000000000, 0.000000000000000000 ) ) ;
#19085=CIRCLE ( 'NONE', #10876, 9.500000000000000000 ) ;
#19099=VECTOR ( 'NONE', #2472, 1000.000000000000000 ) ;
#19123=B_SPLINE_CURVE_WITH_KNOTS ( 'NONE', 3,
 ( #1981, #6774, #556, #13065, #16357, #14688, #5311, #2285, #6867, #13151, #17867, #3764, #2192, #647, #6960, #13243 ),
 .UNSPECIFIED., .F., .F.,
 ( 4, 2, 2, 2, 2, 2, 2, 4 ),
 ( 0.000000000000000000, 0.0005901654530283999755, 0.001180330906056799951, 0.001770496359085199818, 0.002360661812113599902, 0.003540992718170399636, 0.004131158171198803623, 0.004721323624227206743 ),
 .UNSPECIFIED. ) ;
#19147=STYLED_ITEM ( 'NONE', ( #5843 ), #8197 ) ;
#19165=CARTESIAN_POINT ( 'NONE',  ( 0.000000000000000000, 66.00000000000000000, -9.500000000000000000 ) ) ;
#19181=DIRECTION ( 'NONE',  ( -0.000000000000000000, 1.000000000000000000, -0.000000000000000000 ) ) ;
#19203=EDGE_LOOP ( 'NONE', ( #2955, #2367, #9846, #498 ) ) ;
#19258=DIRECTION ( 'NONE',  ( -0.000000000000000000, 1.000000000000000000, -0.000000000000000000 ) ) ;
#19292=DIRECTION ( 'NONE',  ( -0.000000000000000000, -0.000000000000000000, 1.000000000000000000 ) ) ;
#19329=ORIENTED_EDGE ( 'NONE', *, *, #14734, .F. ) ;
#19392=FACE_OUTER_BOUND ( 'NONE', #8729, .T. ) ;
#19398=CARTESIAN_POINT ( 'NONE',  ( -1.224646799147350495E-16, 41.00000000000000711, 6.000000000000000000 ) ) ;
#19421=VERTEX_POINT ( 'NONE', #9287 ) ;
#19513=VECTOR ( 'NONE', #8334, 1000.000000000000000 ) ;
#19524=ADVANCED_FACE ( 'NONE', ( #14437 ), #3626, .T. ) ;
#19536=CARTESIAN_POINT ( 'NONE',  ( 0.000000000000000000, 66.00000000000000000, -5.741599279633704455E-16 ) ) ;
#19632=CARTESIAN_POINT ( 'NONE',  ( 1.469576158976824144E-15, 10.00000000000000000, 12.00000000000000178 ) ) ;
#19652=VECTOR ( 'NONE', #17999, 1000.000000000000114 ) ;
#19732=CARTESIAN_POINT ( 'NONE',  ( 0.000000000000000000, 66.00000000000000000, 0.000000000000000000 ) ) ;
#19735=VERTEX_POINT ( 'NONE', #6438 ) ;
#19752=CONICAL_SURFACE ( 'NONE', #16495, 0.9999999999999950040, 1.029744258676644320 ) ;
#19759=DIRECTION ( 'NONE',  ( -0.000000000000000000, -1.000000000000000000, -0.000000000000000000 ) ) ;
#19817=EDGE_CURVE ( 'NONE', #19735, #14259, #8184, .T. ) ;
#19835=DIRECTION ( 'NONE',  ( -0.000000000000000000, 1.000000000000000000, -0.000000000000000000 ) ) ;
#19881=DIRECTION ( 'NONE',  ( 0.000000000000000000, 1.000000000000000000, 0.000000000000000000 ) ) ;
#19932=FILL_AREA_STYLE_COLOUR ( '', #4679 ) ;
#19935=EDGE_CURVE ( 'NONE', #6580, #13936, #19085, .T. ) ;
#19977=VERTEX_POINT ( 'NONE', #2244 ) ;
#20045=ORIENTED_EDGE ( 'NONE', *, *, #19935, .T. ) ;
#20073=VERTEX_POINT ( 'NONE', #6534 ) ;
#20191=CARTESIAN_POINT ( 'NONE',  ( 0.000000000000000000, 0.000000000000000000, 0.000000000000000000 ) ) ;
#20207=AXIS2_PLACEMENT_3D ( 'NONE', #14646, #12910, #6834 ) ;
#20264=ORIENTED_EDGE ( 'NONE', *, *, #1024, .F. ) ;
#20296=CARTESIAN_POINT ( 'NONE',  ( 0.000000000000000000, 0.000000000000000000, 0.000000000000000000 ) ) ;
ENDSEC;
END-ISO-10303-21;
